ISO-10303-21;
HEADER;
/* Generated by software containing ST-Developer
 * from STEP Tools, Inc. (www.steptools.com) 
 */

FILE_DESCRIPTION(
/* description */ ('PAT-054'),
/* implementation_level */ '2;1');

FILE_NAME(
/* name */ 'Nut bracket.step',
/* time_stamp */ '2026-10-29T16:38:13-07:00',
/* author */ (''),
/* organization */ (''),
/* preprocessor_version */ 'ST-DEVELOPER v20.2',
/* originating_system */ 'Autodesk Translation Framework v15.17.0.0',
/* authorisation */ '');

FILE_SCHEMA (('AUTOMOTIVE_DESIGN { 1 0 10303 214 3 1 1 }'));
ENDSEC;

DATA;
#10=MECHANICAL_DESIGN_GEOMETRIC_PRESENTATION_REPRESENTATION('',(#939),#33981);
#836=SHAPE_REPRESENTATION_RELATIONSHIP('SRR','None',#34212,#880);
#880=ADVANCED_BREP_SHAPE_REPRESENTATION('',(#997),#33960);
#939=STYLED_ITEM('',(#34524),#997);
#997=MANIFOLD_SOLID_BREP('Body1',#13051);
#1176=FACE_BOUND('',#2833,.T.);
#1177=FACE_BOUND('',#2834,.T.);
#1178=FACE_BOUND('',#2835,.T.);
#1179=FACE_BOUND('',#2836,.T.);
#1180=FACE_BOUND('',#2839,.T.);
#1181=FACE_BOUND('',#2841,.T.);
#1182=FACE_BOUND('',#2842,.T.);
#1183=FACE_BOUND('',#2843,.T.);
#1184=FACE_BOUND('',#2844,.T.);
#1424=PLANE('',#14290);
#1425=PLANE('',#14294);
#1426=PLANE('',#14298);
#1427=PLANE('',#14302);
#1428=PLANE('',#14306);
#1429=PLANE('',#14310);
#1430=PLANE('',#14314);
#1431=PLANE('',#14318);
#1432=PLANE('',#14319);
#1433=PLANE('',#14320);
#1434=PLANE('',#14321);
#1435=PLANE('',#14322);
#1436=PLANE('',#14323);
#1929=FACE_OUTER_BOUND('',#2816,.T.);
#1930=FACE_OUTER_BOUND('',#2817,.T.);
#1931=FACE_OUTER_BOUND('',#2818,.T.);
#1932=FACE_OUTER_BOUND('',#2819,.T.);
#1933=FACE_OUTER_BOUND('',#2820,.T.);
#1934=FACE_OUTER_BOUND('',#2821,.T.);
#1935=FACE_OUTER_BOUND('',#2822,.T.);
#1936=FACE_OUTER_BOUND('',#2823,.T.);
#1937=FACE_OUTER_BOUND('',#2824,.T.);
#1938=FACE_OUTER_BOUND('',#2825,.T.);
#1939=FACE_OUTER_BOUND('',#2826,.T.);
#1940=FACE_OUTER_BOUND('',#2827,.T.);
#1941=FACE_OUTER_BOUND('',#2828,.T.);
#1942=FACE_OUTER_BOUND('',#2829,.T.);
#1943=FACE_OUTER_BOUND('',#2830,.T.);
#1944=FACE_OUTER_BOUND('',#2831,.T.);
#1945=FACE_OUTER_BOUND('',#2832,.T.);
#1946=FACE_OUTER_BOUND('',#2837,.T.);
#1947=FACE_OUTER_BOUND('',#2838,.T.);
#1948=FACE_OUTER_BOUND('',#2840,.T.);
#1949=FACE_OUTER_BOUND('',#2845,.T.);
#2816=EDGE_LOOP('',(#10157,#10158,#10159,#10160));
#2817=EDGE_LOOP('',(#10161));
#2818=EDGE_LOOP('',(#10162,#10163,#10164,#10165));
#2819=EDGE_LOOP('',(#10166));
#2820=EDGE_LOOP('',(#10167,#10168,#10169,#10170));
#2821=EDGE_LOOP('',(#10171));
#2822=EDGE_LOOP('',(#10172,#10173,#10174,#10175));
#2823=EDGE_LOOP('',(#10176));
#2824=EDGE_LOOP('',(#10177,#10178,#10179,#10180));
#2825=EDGE_LOOP('',(#10181));
#2826=EDGE_LOOP('',(#10182,#10183,#10184,#10185));
#2827=EDGE_LOOP('',(#10186));
#2828=EDGE_LOOP('',(#10187,#10188,#10189,#10190));
#2829=EDGE_LOOP('',(#10191));
#2830=EDGE_LOOP('',(#10192,#10193,#10194,#10195));
#2831=EDGE_LOOP('',(#10196,#10197,#10198,#10199));
#2832=EDGE_LOOP('',(#10200,#10201,#10202,#10203));
#2833=EDGE_LOOP('',(#10204));
#2834=EDGE_LOOP('',(#10205));
#2835=EDGE_LOOP('',(#10206));
#2836=EDGE_LOOP('',(#10207));
#2837=EDGE_LOOP('',(#10208,#10209,#10210,#10211));
#2838=EDGE_LOOP('',(#10212,#10213,#10214,#10215));
#2839=EDGE_LOOP('',(#10216));
#2840=EDGE_LOOP('',(#10217,#10218,#10219,#10220));
#2841=EDGE_LOOP('',(#10221));
#2842=EDGE_LOOP('',(#10222));
#2843=EDGE_LOOP('',(#10223));
#2844=EDGE_LOOP('',(#10224));
#2845=EDGE_LOOP('',(#10225,#10226,#10227,#10228));
#3706=LINE('',#20923,#4640);
#3707=LINE('',#20930,#4641);
#3708=LINE('',#20937,#4642);
#3709=LINE('',#20944,#4643);
#3710=LINE('',#20951,#4644);
#3711=LINE('',#20958,#4645);
#3712=LINE('',#20965,#4646);
#3713=LINE('',#20972,#4647);
#3714=LINE('',#20977,#4648);
#3715=LINE('',#20979,#4649);
#3716=LINE('',#20981,#4650);
#3717=LINE('',#20982,#4651);
#3718=LINE('',#20985,#4652);
#3719=LINE('',#20987,#4653);
#3720=LINE('',#20988,#4654);
#3721=LINE('',#20991,#4655);
#3722=LINE('',#20993,#4656);
#3723=LINE('',#20994,#4657);
#3724=LINE('',#20996,#4658);
#3725=LINE('',#20997,#4659);
#4640=VECTOR('',#16819,0.210000000000001);
#4641=VECTOR('',#16828,0.210000000000001);
#4642=VECTOR('',#16837,0.210000000000001);
#4643=VECTOR('',#16846,0.210000000000001);
#4644=VECTOR('',#16855,0.165);
#4645=VECTOR('',#16864,0.165);
#4646=VECTOR('',#16873,0.165);
#4647=VECTOR('',#16882,1.11);
#4648=VECTOR('',#16887,1.);
#4649=VECTOR('',#16888,1.);
#4650=VECTOR('',#16889,1.);
#4651=VECTOR('',#16890,1.);
#4652=VECTOR('',#16893,1.);
#4653=VECTOR('',#16894,1.);
#4654=VECTOR('',#16895,1.);
#4655=VECTOR('',#16898,1.);
#4656=VECTOR('',#16899,1.);
#4657=VECTOR('',#16900,1.);
#4658=VECTOR('',#16903,1.);
#4659=VECTOR('',#16904,1.);
#5436=CIRCLE('',#14288,0.210000000000001);
#5437=CIRCLE('',#14289,0.210000000000001);
#5438=CIRCLE('',#14292,0.210000000000001);
#5439=CIRCLE('',#14293,0.210000000000001);
#5440=CIRCLE('',#14296,0.210000000000001);
#5441=CIRCLE('',#14297,0.210000000000001);
#5442=CIRCLE('',#14300,0.210000000000001);
#5443=CIRCLE('',#14301,0.210000000000001);
#5444=CIRCLE('',#14304,0.165);
#5445=CIRCLE('',#14305,0.165);
#5446=CIRCLE('',#14308,0.165);
#5447=CIRCLE('',#14309,0.165);
#5448=CIRCLE('',#14312,0.165);
#5449=CIRCLE('',#14313,0.165);
#5450=CIRCLE('',#14316,1.11);
#5451=CIRCLE('',#14317,1.11);
#6142=VERTEX_POINT('',#20920);
#6143=VERTEX_POINT('',#20922);
#6144=VERTEX_POINT('',#20927);
#6145=VERTEX_POINT('',#20929);
#6146=VERTEX_POINT('',#20934);
#6147=VERTEX_POINT('',#20936);
#6148=VERTEX_POINT('',#20941);
#6149=VERTEX_POINT('',#20943);
#6150=VERTEX_POINT('',#20948);
#6151=VERTEX_POINT('',#20950);
#6152=VERTEX_POINT('',#20955);
#6153=VERTEX_POINT('',#20957);
#6154=VERTEX_POINT('',#20962);
#6155=VERTEX_POINT('',#20964);
#6156=VERTEX_POINT('',#20969);
#6157=VERTEX_POINT('',#20971);
#6158=VERTEX_POINT('',#20975);
#6159=VERTEX_POINT('',#20976);
#6160=VERTEX_POINT('',#20978);
#6161=VERTEX_POINT('',#20980);
#6162=VERTEX_POINT('',#20984);
#6163=VERTEX_POINT('',#20986);
#6164=VERTEX_POINT('',#20990);
#6165=VERTEX_POINT('',#20992);
#7578=EDGE_CURVE('',#6142,#6142,#5436,.T.);
#7579=EDGE_CURVE('',#6142,#6143,#3706,.T.);
#7580=EDGE_CURVE('',#6143,#6143,#5437,.T.);
#7581=EDGE_CURVE('',#6144,#6144,#5438,.T.);
#7582=EDGE_CURVE('',#6144,#6145,#3707,.T.);
#7583=EDGE_CURVE('',#6145,#6145,#5439,.T.);
#7584=EDGE_CURVE('',#6146,#6146,#5440,.T.);
#7585=EDGE_CURVE('',#6146,#6147,#3708,.T.);
#7586=EDGE_CURVE('',#6147,#6147,#5441,.T.);
#7587=EDGE_CURVE('',#6148,#6148,#5442,.T.);
#7588=EDGE_CURVE('',#6148,#6149,#3709,.T.);
#7589=EDGE_CURVE('',#6149,#6149,#5443,.T.);
#7590=EDGE_CURVE('',#6150,#6150,#5444,.T.);
#7591=EDGE_CURVE('',#6150,#6151,#3710,.T.);
#7592=EDGE_CURVE('',#6151,#6151,#5445,.T.);
#7593=EDGE_CURVE('',#6152,#6152,#5446,.T.);
#7594=EDGE_CURVE('',#6152,#6153,#3711,.T.);
#7595=EDGE_CURVE('',#6153,#6153,#5447,.T.);
#7596=EDGE_CURVE('',#6154,#6154,#5448,.T.);
#7597=EDGE_CURVE('',#6154,#6155,#3712,.T.);
#7598=EDGE_CURVE('',#6155,#6155,#5449,.T.);
#7599=EDGE_CURVE('',#6156,#6156,#5450,.T.);
#7600=EDGE_CURVE('',#6156,#6157,#3713,.T.);
#7601=EDGE_CURVE('',#6157,#6157,#5451,.T.);
#7602=EDGE_CURVE('',#6158,#6159,#3714,.T.);
#7603=EDGE_CURVE('',#6159,#6160,#3715,.T.);
#7604=EDGE_CURVE('',#6161,#6160,#3716,.T.);
#7605=EDGE_CURVE('',#6158,#6161,#3717,.T.);
#7606=EDGE_CURVE('',#6162,#6158,#3718,.T.);
#7607=EDGE_CURVE('',#6163,#6161,#3719,.T.);
#7608=EDGE_CURVE('',#6162,#6163,#3720,.T.);
#7609=EDGE_CURVE('',#6164,#6162,#3721,.T.);
#7610=EDGE_CURVE('',#6165,#6163,#3722,.T.);
#7611=EDGE_CURVE('',#6164,#6165,#3723,.T.);
#7612=EDGE_CURVE('',#6159,#6164,#3724,.T.);
#7613=EDGE_CURVE('',#6160,#6165,#3725,.T.);
#10157=ORIENTED_EDGE('',*,*,#7578,.F.);
#10158=ORIENTED_EDGE('',*,*,#7579,.T.);
#10159=ORIENTED_EDGE('',*,*,#7580,.F.);
#10160=ORIENTED_EDGE('',*,*,#7579,.F.);
#10161=ORIENTED_EDGE('',*,*,#7578,.T.);
#10162=ORIENTED_EDGE('',*,*,#7581,.F.);
#10163=ORIENTED_EDGE('',*,*,#7582,.T.);
#10164=ORIENTED_EDGE('',*,*,#7583,.F.);
#10165=ORIENTED_EDGE('',*,*,#7582,.F.);
#10166=ORIENTED_EDGE('',*,*,#7581,.T.);
#10167=ORIENTED_EDGE('',*,*,#7584,.F.);
#10168=ORIENTED_EDGE('',*,*,#7585,.T.);
#10169=ORIENTED_EDGE('',*,*,#7586,.F.);
#10170=ORIENTED_EDGE('',*,*,#7585,.F.);
#10171=ORIENTED_EDGE('',*,*,#7584,.T.);
#10172=ORIENTED_EDGE('',*,*,#7587,.F.);
#10173=ORIENTED_EDGE('',*,*,#7588,.T.);
#10174=ORIENTED_EDGE('',*,*,#7589,.F.);
#10175=ORIENTED_EDGE('',*,*,#7588,.F.);
#10176=ORIENTED_EDGE('',*,*,#7587,.T.);
#10177=ORIENTED_EDGE('',*,*,#7590,.F.);
#10178=ORIENTED_EDGE('',*,*,#7591,.T.);
#10179=ORIENTED_EDGE('',*,*,#7592,.F.);
#10180=ORIENTED_EDGE('',*,*,#7591,.F.);
#10181=ORIENTED_EDGE('',*,*,#7590,.T.);
#10182=ORIENTED_EDGE('',*,*,#7593,.F.);
#10183=ORIENTED_EDGE('',*,*,#7594,.T.);
#10184=ORIENTED_EDGE('',*,*,#7595,.F.);
#10185=ORIENTED_EDGE('',*,*,#7594,.F.);
#10186=ORIENTED_EDGE('',*,*,#7593,.T.);
#10187=ORIENTED_EDGE('',*,*,#7596,.F.);
#10188=ORIENTED_EDGE('',*,*,#7597,.T.);
#10189=ORIENTED_EDGE('',*,*,#7598,.F.);
#10190=ORIENTED_EDGE('',*,*,#7597,.F.);
#10191=ORIENTED_EDGE('',*,*,#7596,.T.);
#10192=ORIENTED_EDGE('',*,*,#7599,.F.);
#10193=ORIENTED_EDGE('',*,*,#7600,.T.);
#10194=ORIENTED_EDGE('',*,*,#7601,.F.);
#10195=ORIENTED_EDGE('',*,*,#7600,.F.);
#10196=ORIENTED_EDGE('',*,*,#7602,.T.);
#10197=ORIENTED_EDGE('',*,*,#7603,.T.);
#10198=ORIENTED_EDGE('',*,*,#7604,.F.);
#10199=ORIENTED_EDGE('',*,*,#7605,.F.);
#10200=ORIENTED_EDGE('',*,*,#7606,.T.);
#10201=ORIENTED_EDGE('',*,*,#7605,.T.);
#10202=ORIENTED_EDGE('',*,*,#7607,.F.);
#10203=ORIENTED_EDGE('',*,*,#7608,.F.);
#10204=ORIENTED_EDGE('',*,*,#7592,.T.);
#10205=ORIENTED_EDGE('',*,*,#7595,.T.);
#10206=ORIENTED_EDGE('',*,*,#7598,.T.);
#10207=ORIENTED_EDGE('',*,*,#7601,.T.);
#10208=ORIENTED_EDGE('',*,*,#7609,.T.);
#10209=ORIENTED_EDGE('',*,*,#7608,.T.);
#10210=ORIENTED_EDGE('',*,*,#7610,.F.);
#10211=ORIENTED_EDGE('',*,*,#7611,.F.);
#10212=ORIENTED_EDGE('',*,*,#7612,.T.);
#10213=ORIENTED_EDGE('',*,*,#7611,.T.);
#10214=ORIENTED_EDGE('',*,*,#7613,.F.);
#10215=ORIENTED_EDGE('',*,*,#7603,.F.);
#10216=ORIENTED_EDGE('',*,*,#7599,.T.);
#10217=ORIENTED_EDGE('',*,*,#7613,.T.);
#10218=ORIENTED_EDGE('',*,*,#7610,.T.);
#10219=ORIENTED_EDGE('',*,*,#7607,.T.);
#10220=ORIENTED_EDGE('',*,*,#7604,.T.);
#10221=ORIENTED_EDGE('',*,*,#7580,.T.);
#10222=ORIENTED_EDGE('',*,*,#7583,.T.);
#10223=ORIENTED_EDGE('',*,*,#7586,.T.);
#10224=ORIENTED_EDGE('',*,*,#7589,.T.);
#10225=ORIENTED_EDGE('',*,*,#7612,.F.);
#10226=ORIENTED_EDGE('',*,*,#7602,.F.);
#10227=ORIENTED_EDGE('',*,*,#7606,.F.);
#10228=ORIENTED_EDGE('',*,*,#7609,.F.);
#12091=CYLINDRICAL_SURFACE('',#14287,0.210000000000001);
#12092=CYLINDRICAL_SURFACE('',#14291,0.210000000000001);
#12093=CYLINDRICAL_SURFACE('',#14295,0.210000000000001);
#12094=CYLINDRICAL_SURFACE('',#14299,0.210000000000001);
#12095=CYLINDRICAL_SURFACE('',#14303,0.165);
#12096=CYLINDRICAL_SURFACE('',#14307,0.165);
#12097=CYLINDRICAL_SURFACE('',#14311,0.165);
#12098=CYLINDRICAL_SURFACE('',#14315,1.11);
#12641=ADVANCED_FACE('',(#1929),#12091,.F.);
#12642=ADVANCED_FACE('',(#1930),#1424,.T.);
#12643=ADVANCED_FACE('',(#1931),#12092,.F.);
#12644=ADVANCED_FACE('',(#1932),#1425,.T.);
#12645=ADVANCED_FACE('',(#1933),#12093,.F.);
#12646=ADVANCED_FACE('',(#1934),#1426,.T.);
#12647=ADVANCED_FACE('',(#1935),#12094,.F.);
#12648=ADVANCED_FACE('',(#1936),#1427,.T.);
#12649=ADVANCED_FACE('',(#1937),#12095,.F.);
#12650=ADVANCED_FACE('',(#1938),#1428,.T.);
#12651=ADVANCED_FACE('',(#1939),#12096,.F.);
#12652=ADVANCED_FACE('',(#1940),#1429,.T.);
#12653=ADVANCED_FACE('',(#1941),#12097,.F.);
#12654=ADVANCED_FACE('',(#1942),#1430,.T.);
#12655=ADVANCED_FACE('',(#1943),#12098,.F.);
#12656=ADVANCED_FACE('',(#1944),#1431,.T.);
#12657=ADVANCED_FACE('',(#1945,#1176,#1177,#1178,#1179),#1432,.T.);
#12658=ADVANCED_FACE('',(#1946),#1433,.T.);
#12659=ADVANCED_FACE('',(#1947,#1180),#1434,.T.);
#12660=ADVANCED_FACE('',(#1948,#1181,#1182,#1183,#1184),#1435,.T.);
#12661=ADVANCED_FACE('',(#1949),#1436,.F.);
#13051=CLOSED_SHELL('',(#12641,#12642,#12643,#12644,#12645,#12646,#12647,
#12648,#12649,#12650,#12651,#12652,#12653,#12654,#12655,#12656,#12657,#12658,
#12659,#12660,#12661));
#14286=AXIS2_PLACEMENT_3D('',#20918,#16813,#16814);
#14287=AXIS2_PLACEMENT_3D('',#20919,#16815,#16816);
#14288=AXIS2_PLACEMENT_3D('',#20921,#16817,#16818);
#14289=AXIS2_PLACEMENT_3D('',#20924,#16820,#16821);
#14290=AXIS2_PLACEMENT_3D('',#20925,#16822,#16823);
#14291=AXIS2_PLACEMENT_3D('',#20926,#16824,#16825);
#14292=AXIS2_PLACEMENT_3D('',#20928,#16826,#16827);
#14293=AXIS2_PLACEMENT_3D('',#20931,#16829,#16830);
#14294=AXIS2_PLACEMENT_3D('',#20932,#16831,#16832);
#14295=AXIS2_PLACEMENT_3D('',#20933,#16833,#16834);
#14296=AXIS2_PLACEMENT_3D('',#20935,#16835,#16836);
#14297=AXIS2_PLACEMENT_3D('',#20938,#16838,#16839);
#14298=AXIS2_PLACEMENT_3D('',#20939,#16840,#16841);
#14299=AXIS2_PLACEMENT_3D('',#20940,#16842,#16843);
#14300=AXIS2_PLACEMENT_3D('',#20942,#16844,#16845);
#14301=AXIS2_PLACEMENT_3D('',#20945,#16847,#16848);
#14302=AXIS2_PLACEMENT_3D('',#20946,#16849,#16850);
#14303=AXIS2_PLACEMENT_3D('',#20947,#16851,#16852);
#14304=AXIS2_PLACEMENT_3D('',#20949,#16853,#16854);
#14305=AXIS2_PLACEMENT_3D('',#20952,#16856,#16857);
#14306=AXIS2_PLACEMENT_3D('',#20953,#16858,#16859);
#14307=AXIS2_PLACEMENT_3D('',#20954,#16860,#16861);
#14308=AXIS2_PLACEMENT_3D('',#20956,#16862,#16863);
#14309=AXIS2_PLACEMENT_3D('',#20959,#16865,#16866);
#14310=AXIS2_PLACEMENT_3D('',#20960,#16867,#16868);
#14311=AXIS2_PLACEMENT_3D('',#20961,#16869,#16870);
#14312=AXIS2_PLACEMENT_3D('',#20963,#16871,#16872);
#14313=AXIS2_PLACEMENT_3D('',#20966,#16874,#16875);
#14314=AXIS2_PLACEMENT_3D('',#20967,#16876,#16877);
#14315=AXIS2_PLACEMENT_3D('',#20968,#16878,#16879);
#14316=AXIS2_PLACEMENT_3D('',#20970,#16880,#16881);
#14317=AXIS2_PLACEMENT_3D('',#20973,#16883,#16884);
#14318=AXIS2_PLACEMENT_3D('',#20974,#16885,#16886);
#14319=AXIS2_PLACEMENT_3D('',#20983,#16891,#16892);
#14320=AXIS2_PLACEMENT_3D('',#20989,#16896,#16897);
#14321=AXIS2_PLACEMENT_3D('',#20995,#16901,#16902);
#14322=AXIS2_PLACEMENT_3D('',#20998,#16905,#16906);
#14323=AXIS2_PLACEMENT_3D('',#20999,#16907,#16908);
#16813=DIRECTION('axis',(0.,0.,1.));
#16814=DIRECTION('refdir',(1.,0.,0.));
#16815=DIRECTION('center_axis',(0.,0.,1.));
#16816=DIRECTION('ref_axis',(1.,0.,0.));
#16817=DIRECTION('center_axis',(0.,0.,1.));
#16818=DIRECTION('ref_axis',(1.,0.,0.));
#16819=DIRECTION('',(0.,0.,1.));
#16820=DIRECTION('center_axis',(0.,0.,-1.));
#16821=DIRECTION('ref_axis',(1.,0.,0.));
#16822=DIRECTION('center_axis',(0.,0.,1.));
#16823=DIRECTION('ref_axis',(1.,0.,0.));
#16824=DIRECTION('center_axis',(0.,0.,1.));
#16825=DIRECTION('ref_axis',(1.,0.,0.));
#16826=DIRECTION('center_axis',(0.,0.,1.));
#16827=DIRECTION('ref_axis',(1.,0.,0.));
#16828=DIRECTION('',(0.,0.,1.));
#16829=DIRECTION('center_axis',(0.,0.,-1.));
#16830=DIRECTION('ref_axis',(1.,0.,0.));
#16831=DIRECTION('center_axis',(0.,0.,1.));
#16832=DIRECTION('ref_axis',(1.,0.,0.));
#16833=DIRECTION('center_axis',(0.,0.,1.));
#16834=DIRECTION('ref_axis',(1.,0.,0.));
#16835=DIRECTION('center_axis',(0.,0.,1.));
#16836=DIRECTION('ref_axis',(1.,0.,0.));
#16837=DIRECTION('',(0.,0.,1.));
#16838=DIRECTION('center_axis',(0.,0.,-1.));
#16839=DIRECTION('ref_axis',(1.,0.,0.));
#16840=DIRECTION('center_axis',(0.,0.,1.));
#16841=DIRECTION('ref_axis',(1.,0.,0.));
#16842=DIRECTION('center_axis',(0.,0.,1.));
#16843=DIRECTION('ref_axis',(1.,0.,0.));
#16844=DIRECTION('center_axis',(0.,0.,1.));
#16845=DIRECTION('ref_axis',(1.,0.,0.));
#16846=DIRECTION('',(0.,0.,1.));
#16847=DIRECTION('center_axis',(0.,0.,-1.));
#16848=DIRECTION('ref_axis',(1.,0.,0.));
#16849=DIRECTION('center_axis',(0.,0.,1.));
#16850=DIRECTION('ref_axis',(1.,0.,0.));
#16851=DIRECTION('center_axis',(1.,0.,0.));
#16852=DIRECTION('ref_axis',(0.,0.,-1.));
#16853=DIRECTION('center_axis',(1.,0.,0.));
#16854=DIRECTION('ref_axis',(0.,0.,-1.));
#16855=DIRECTION('',(1.,0.,0.));
#16856=DIRECTION('center_axis',(-1.,0.,0.));
#16857=DIRECTION('ref_axis',(0.,0.,-1.));
#16858=DIRECTION('center_axis',(1.,0.,0.));
#16859=DIRECTION('ref_axis',(0.,0.,-1.));
#16860=DIRECTION('center_axis',(1.,0.,0.));
#16861=DIRECTION('ref_axis',(0.,0.,-1.));
#16862=DIRECTION('center_axis',(1.,0.,0.));
#16863=DIRECTION('ref_axis',(0.,0.,-1.));
#16864=DIRECTION('',(1.,0.,0.));
#16865=DIRECTION('center_axis',(-1.,0.,0.));
#16866=DIRECTION('ref_axis',(0.,0.,-1.));
#16867=DIRECTION('center_axis',(1.,0.,0.));
#16868=DIRECTION('ref_axis',(0.,0.,-1.));
#16869=DIRECTION('center_axis',(1.,0.,0.));
#16870=DIRECTION('ref_axis',(0.,0.,-1.));
#16871=DIRECTION('center_axis',(1.,0.,0.));
#16872=DIRECTION('ref_axis',(0.,0.,-1.));
#16873=DIRECTION('',(1.,0.,0.));
#16874=DIRECTION('center_axis',(-1.,0.,0.));
#16875=DIRECTION('ref_axis',(0.,0.,-1.));
#16876=DIRECTION('center_axis',(1.,0.,0.));
#16877=DIRECTION('ref_axis',(0.,0.,-1.));
#16878=DIRECTION('center_axis',(1.,0.,0.));
#16879=DIRECTION('ref_axis',(0.,0.,-1.));
#16880=DIRECTION('center_axis',(1.,0.,0.));
#16881=DIRECTION('ref_axis',(0.,0.,-1.));
#16882=DIRECTION('',(1.,0.,0.));
#16883=DIRECTION('center_axis',(-1.,0.,0.));
#16884=DIRECTION('ref_axis',(0.,0.,-1.));
#16885=DIRECTION('center_axis',(0.,1.,0.));
#16886=DIRECTION('ref_axis',(-1.,0.,0.));
#16887=DIRECTION('',(-1.,0.,0.));
#16888=DIRECTION('',(0.,0.,1.));
#16889=DIRECTION('',(-1.,0.,0.));
#16890=DIRECTION('',(0.,0.,1.));
#16891=DIRECTION('center_axis',(1.,0.,0.));
#16892=DIRECTION('ref_axis',(0.,1.,0.));
#16893=DIRECTION('',(0.,1.,0.));
#16894=DIRECTION('',(0.,1.,0.));
#16895=DIRECTION('',(0.,0.,1.));
#16896=DIRECTION('center_axis',(0.,-1.,0.));
#16897=DIRECTION('ref_axis',(1.,0.,0.));
#16898=DIRECTION('',(1.,0.,0.));
#16899=DIRECTION('',(1.,0.,0.));
#16900=DIRECTION('',(0.,0.,1.));
#16901=DIRECTION('center_axis',(-1.,0.,0.));
#16902=DIRECTION('ref_axis',(0.,-1.,0.));
#16903=DIRECTION('',(0.,-1.,0.));
#16904=DIRECTION('',(0.,-1.,0.));
#16905=DIRECTION('center_axis',(0.,0.,1.));
#16906=DIRECTION('ref_axis',(1.,0.,0.));
#16907=DIRECTION('center_axis',(0.,0.,1.));
#16908=DIRECTION('ref_axis',(1.,0.,0.));
#20918=CARTESIAN_POINT('',(0.,0.,0.));
#20919=CARTESIAN_POINT('Origin',(14.,-1.5,5.1));
#20920=CARTESIAN_POINT('',(13.79,-1.5,5.1));
#20921=CARTESIAN_POINT('Origin',(14.,-1.5,5.1));
#20922=CARTESIAN_POINT('',(13.79,-1.5,6.));
#20923=CARTESIAN_POINT('',(13.79,-1.5,5.1));
#20924=CARTESIAN_POINT('Origin',(14.,-1.5,6.));
#20925=CARTESIAN_POINT('Origin',(14.,-1.5,5.1));
#20926=CARTESIAN_POINT('Origin',(12.5,1.5,5.1));
#20927=CARTESIAN_POINT('',(12.29,1.5,5.1));
#20928=CARTESIAN_POINT('Origin',(12.5,1.5,5.1));
#20929=CARTESIAN_POINT('',(12.29,1.5,6.));
#20930=CARTESIAN_POINT('',(12.29,1.5,5.1));
#20931=CARTESIAN_POINT('Origin',(12.5,1.5,6.));
#20932=CARTESIAN_POINT('Origin',(12.5,1.5,5.1));
#20933=CARTESIAN_POINT('Origin',(12.5,-1.5,5.1));
#20934=CARTESIAN_POINT('',(12.29,-1.5,5.1));
#20935=CARTESIAN_POINT('Origin',(12.5,-1.5,5.1));
#20936=CARTESIAN_POINT('',(12.29,-1.5,6.));
#20937=CARTESIAN_POINT('',(12.29,-1.5,5.1));
#20938=CARTESIAN_POINT('Origin',(12.5,-1.5,6.));
#20939=CARTESIAN_POINT('Origin',(12.5,-1.5,5.1));
#20940=CARTESIAN_POINT('Origin',(14.,1.5,5.1));
#20941=CARTESIAN_POINT('',(13.79,1.5,5.1));
#20942=CARTESIAN_POINT('Origin',(14.,1.5,5.1));
#20943=CARTESIAN_POINT('',(13.79,1.5,6.));
#20944=CARTESIAN_POINT('',(13.79,1.5,5.1));
#20945=CARTESIAN_POINT('Origin',(14.,1.5,6.));
#20946=CARTESIAN_POINT('Origin',(14.,1.5,5.1));
#20947=CARTESIAN_POINT('Origin',(12.9,-1.5,4.));
#20948=CARTESIAN_POINT('',(12.9,-1.5,4.165));
#20949=CARTESIAN_POINT('Origin',(12.9,-1.5,4.));
#20950=CARTESIAN_POINT('',(14.5,-1.5,4.165));
#20951=CARTESIAN_POINT('',(12.9,-1.5,4.165));
#20952=CARTESIAN_POINT('Origin',(14.5,-1.5,4.));
#20953=CARTESIAN_POINT('Origin',(12.9,-1.5,4.));
#20954=CARTESIAN_POINT('Origin',(12.9,1.5,4.));
#20955=CARTESIAN_POINT('',(12.9,1.5,4.165));
#20956=CARTESIAN_POINT('Origin',(12.9,1.5,4.));
#20957=CARTESIAN_POINT('',(14.5,1.5,4.165));
#20958=CARTESIAN_POINT('',(12.9,1.5,4.165));
#20959=CARTESIAN_POINT('Origin',(14.5,1.5,4.));
#20960=CARTESIAN_POINT('Origin',(12.9,1.5,4.));
#20961=CARTESIAN_POINT('Origin',(12.9,0.,5.5));
#20962=CARTESIAN_POINT('',(12.9,-2.02066721859313E-17,5.665));
#20963=CARTESIAN_POINT('Origin',(12.9,0.,5.5));
#20964=CARTESIAN_POINT('',(14.5,2.02066721859313E-17,5.665));
#20965=CARTESIAN_POINT('',(12.9,-2.02066721859313E-17,5.665));
#20966=CARTESIAN_POINT('Origin',(14.5,0.,5.5));
#20967=CARTESIAN_POINT('Origin',(12.9,0.,5.5));
#20968=CARTESIAN_POINT('Origin',(11.9,0.,4.));
#20969=CARTESIAN_POINT('',(12.,-1.35935794705356E-16,5.11));
#20970=CARTESIAN_POINT('Origin',(12.,0.,4.));
#20971=CARTESIAN_POINT('',(14.5,1.35935794705356E-16,5.11));
#20972=CARTESIAN_POINT('',(11.9,-1.35935794705356E-16,5.11));
#20973=CARTESIAN_POINT('Origin',(14.5,0.,4.));
#20974=CARTESIAN_POINT('Origin',(14.5,2.2,2.5));
#20975=CARTESIAN_POINT('',(14.5,2.2,2.5));
#20976=CARTESIAN_POINT('',(12.,2.2,2.5));
#20977=CARTESIAN_POINT('',(14.5,2.2,2.5));
#20978=CARTESIAN_POINT('',(12.,2.2,6.));
#20979=CARTESIAN_POINT('',(12.,2.2,2.5));
#20980=CARTESIAN_POINT('',(14.5,2.2,6.));
#20981=CARTESIAN_POINT('',(14.5,2.2,6.));
#20982=CARTESIAN_POINT('',(14.5,2.2,2.5));
#20983=CARTESIAN_POINT('Origin',(14.5,-2.2,2.5));
#20984=CARTESIAN_POINT('',(14.5,-2.2,2.5));
#20985=CARTESIAN_POINT('',(14.5,-2.2,2.5));
#20986=CARTESIAN_POINT('',(14.5,-2.2,6.));
#20987=CARTESIAN_POINT('',(14.5,-2.2,6.));
#20988=CARTESIAN_POINT('',(14.5,-2.2,2.5));
#20989=CARTESIAN_POINT('Origin',(12.,-2.2,2.5));
#20990=CARTESIAN_POINT('',(12.,-2.2,2.5));
#20991=CARTESIAN_POINT('',(12.,-2.2,2.5));
#20992=CARTESIAN_POINT('',(12.,-2.2,6.));
#20993=CARTESIAN_POINT('',(12.,-2.2,6.));
#20994=CARTESIAN_POINT('',(12.,-2.2,2.5));
#20995=CARTESIAN_POINT('Origin',(12.,2.2,2.5));
#20996=CARTESIAN_POINT('',(12.,2.2,2.5));
#20997=CARTESIAN_POINT('',(12.,2.2,6.));
#20998=CARTESIAN_POINT('Origin',(13.25,0.,6.));
#20999=CARTESIAN_POINT('Origin',(13.25,0.,2.5));
#33908=UNCERTAINTY_MEASURE_WITH_UNIT(LENGTH_MEASURE(0.001),#33982,
'DISTANCE_ACCURACY_VALUE',
'Maximum model space distance between geometric entities at asserted c
onnectivities');
#33929=UNCERTAINTY_MEASURE_WITH_UNIT(LENGTH_MEASURE(0.001),#33982,
'DISTANCE_ACCURACY_VALUE',
'Maximum model space distance between geometric entities at asserted c
onnectivities');
#33960=(
GEOMETRIC_REPRESENTATION_CONTEXT(3)
GLOBAL_UNCERTAINTY_ASSIGNED_CONTEXT((#33908))
GLOBAL_UNIT_ASSIGNED_CONTEXT((#33982,#33984,#33985))
REPRESENTATION_CONTEXT('','3D')
);
#33981=(
GEOMETRIC_REPRESENTATION_CONTEXT(3)
GLOBAL_UNCERTAINTY_ASSIGNED_CONTEXT((#33929))
GLOBAL_UNIT_ASSIGNED_CONTEXT((#33982,#33984,#33985))
REPRESENTATION_CONTEXT('','3D')
);
#33982=(
LENGTH_UNIT()
NAMED_UNIT(*)
SI_UNIT(.CENTI.,.METRE.)
);
#33984=(
NAMED_UNIT(*)
PLANE_ANGLE_UNIT()
SI_UNIT($,.RADIAN.)
);
#33985=(
NAMED_UNIT(*)
SI_UNIT($,.STERADIAN.)
SOLID_ANGLE_UNIT()
);
#34016=SHAPE_DEFINITION_REPRESENTATION(#34077,#34212);
#34077=PRODUCT_DEFINITION_SHAPE('',$,#34264);
#34212=SHAPE_REPRESENTATION('',(#14286),#33960);
#34233=PRODUCT_DEFINITION_CONTEXT('part definition',#34388,'design');
#34264=PRODUCT_DEFINITION('Nut bracket','Nut bracket',#34315,#34233);
#34315=PRODUCT_DEFINITION_FORMATION('',$,#34420);
#34388=APPLICATION_CONTEXT(
'Core Data for Automotive Mechanical Design Process');
#34389=PRODUCT_CONTEXT('part definition',#34388,'mechanical');
#34420=PRODUCT('Nut bracket','Nut bracket','Nut bracket',(#34389));
#34518=COLOUR_RGB('Black',0.12,0.14,0.17);
#34519=FILL_AREA_STYLE_COLOUR('',#34518);
#34520=FILL_AREA_STYLE('',(#34519));
#34521=SURFACE_STYLE_FILL_AREA(#34520);
#34522=SURFACE_SIDE_STYLE('',(#34521));
#34523=SURFACE_STYLE_USAGE(.BOTH.,#34522);
#34524=PRESENTATION_STYLE_ASSIGNMENT((#34523));
ENDSEC;
END-ISO-10303-21;
